ISO-10303-21;
HEADER;
/* Generated by software containing ST-Developer
 * from STEP Tools, Inc. (www.steptools.com) 
 */

FILE_DESCRIPTION(
/* description */ ('STEP AP214'),
/* implementation_level */ '2;1');

FILE_NAME(
/* name */ 'Socket Head Cap Screw M4x20.step',
/* time_stamp */ '2026-11-15T14:55:55-08:00',
/* author */ (''),
/* organization */ (''),
/* preprocessor_version */ 'ST-DEVELOPER v20.2',
/* originating_system */ 'Autodesk Translation Framework v15.17.0.0',
/* authorisation */ '');

FILE_SCHEMA (('AUTOMOTIVE_DESIGN { 1 0 10303 214 3 1 1 }'));
ENDSEC;

DATA;
#10=MECHANICAL_DESIGN_GEOMETRIC_PRESENTATION_REPRESENTATION('',(#962),#57079);
#896=SHAPE_REPRESENTATION_RELATIONSHIP('SRR','None',#57286,#925);
#925=ADVANCED_BREP_SHAPE_REPRESENTATION('',(#999),#57078);
#962=STYLED_ITEM('',(#57444),#999);
#999=MANIFOLD_SOLID_BREP('Body1',#24562);
#1340=FACE_BOUND('',#5241,.T.);
#1341=FACE_BOUND('',#5243,.T.);
#2095=PLANE('',#27404);
#2096=PLANE('',#27405);
#2097=PLANE('',#27406);
#2098=PLANE('',#27407);
#2099=PLANE('',#27408);
#2100=PLANE('',#27409);
#2101=PLANE('',#27410);
#2102=PLANE('',#27411);
#2103=PLANE('',#27412);
#2104=PLANE('',#27413);
#2157=CONICAL_SURFACE('',#27396,3.5,0.785398163397447);
#2158=CONICAL_SURFACE('',#27398,1.621,0.785398163397443);
#3520=FACE_OUTER_BOUND('',#5235,.T.);
#3521=FACE_OUTER_BOUND('',#5236,.T.);
#3522=FACE_OUTER_BOUND('',#5237,.T.);
#3523=FACE_OUTER_BOUND('',#5238,.T.);
#3524=FACE_OUTER_BOUND('',#5239,.T.);
#3525=FACE_OUTER_BOUND('',#5240,.T.);
#3526=FACE_OUTER_BOUND('',#5242,.T.);
#3527=FACE_OUTER_BOUND('',#5244,.T.);
#3528=FACE_OUTER_BOUND('',#5245,.T.);
#3529=FACE_OUTER_BOUND('',#5246,.T.);
#3530=FACE_OUTER_BOUND('',#5247,.T.);
#3531=FACE_OUTER_BOUND('',#5248,.T.);
#3532=FACE_OUTER_BOUND('',#5249,.T.);
#3533=FACE_OUTER_BOUND('',#5250,.T.);
#5235=EDGE_LOOP('',(#22684,#22685,#22686,#22687));
#5236=EDGE_LOOP('',(#22688,#22689,#22690,#22691));
#5237=EDGE_LOOP('',(#22692,#22693,#22694,#22695,#22696));
#5238=EDGE_LOOP('',(#22697,#22698,#22699,#22700,#22701));
#5239=EDGE_LOOP('',(#22702));
#5240=EDGE_LOOP('',(#22703));
#5241=EDGE_LOOP('',(#22704,#22705,#22706,#22707,#22708,#22709));
#5242=EDGE_LOOP('',(#22710));
#5243=EDGE_LOOP('',(#22711));
#5244=EDGE_LOOP('',(#22712,#22713,#22714,#22715));
#5245=EDGE_LOOP('',(#22716,#22717,#22718,#22719));
#5246=EDGE_LOOP('',(#22720,#22721,#22722,#22723));
#5247=EDGE_LOOP('',(#22724,#22725,#22726,#22727));
#5248=EDGE_LOOP('',(#22728,#22729,#22730,#22731));
#5249=EDGE_LOOP('',(#22732,#22733,#22734,#22735));
#5250=EDGE_LOOP('',(#22736,#22737,#22738,#22739,#22740,#22741));
#7196=LINE('',#56881,#9163);
#7197=LINE('',#56885,#9164);
#7198=LINE('',#56892,#9165);
#7199=LINE('',#56897,#9166);
#7200=LINE('',#56903,#9167);
#7201=LINE('',#56905,#9168);
#7202=LINE('',#56907,#9169);
#7203=LINE('',#56909,#9170);
#7204=LINE('',#56911,#9171);
#7205=LINE('',#56912,#9172);
#7206=LINE('',#56916,#9173);
#7207=LINE('',#56918,#9174);
#7208=LINE('',#56919,#9175);
#7209=LINE('',#56922,#9176);
#7210=LINE('',#56923,#9177);
#7211=LINE('',#56926,#9178);
#7212=LINE('',#56927,#9179);
#7213=LINE('',#56930,#9180);
#7214=LINE('',#56931,#9181);
#7215=LINE('',#56934,#9182);
#7216=LINE('',#56935,#9183);
#7217=LINE('',#56937,#9184);
#9163=VECTOR('',#34446,3.5);
#9164=VECTOR('',#34451,3.5);
#9165=VECTOR('',#34458,1.621);
#9166=VECTOR('',#34465,2.);
#9167=VECTOR('',#34472,1000.);
#9168=VECTOR('',#34473,1000.);
#9169=VECTOR('',#34474,1000.);
#9170=VECTOR('',#34475,1000.);
#9171=VECTOR('',#34476,1000.);
#9172=VECTOR('',#34477,1000.);
#9173=VECTOR('',#34482,1000.);
#9174=VECTOR('',#34483,1000.);
#9175=VECTOR('',#34484,1000.);
#9176=VECTOR('',#34487,1000.);
#9177=VECTOR('',#34488,1000.);
#9178=VECTOR('',#34491,1000.);
#9179=VECTOR('',#34492,1000.);
#9180=VECTOR('',#34495,1000.);
#9181=VECTOR('',#34496,1000.);
#9182=VECTOR('',#34499,1000.);
#9183=VECTOR('',#34500,1000.);
#9184=VECTOR('',#34503,1000.);
#10272=CIRCLE('',#27394,3.5);
#10273=CIRCLE('',#27395,3.5);
#10274=CIRCLE('',#27397,3.1);
#10275=CIRCLE('',#27399,2.);
#10276=CIRCLE('',#27400,1.621);
#10277=CIRCLE('',#27401,2.);
#10278=CIRCLE('',#27403,2.);
#12484=VERTEX_POINT('',#56878);
#12485=VERTEX_POINT('',#56880);
#12486=VERTEX_POINT('',#56884);
#12487=VERTEX_POINT('',#56888);
#12488=VERTEX_POINT('',#56889);
#12489=VERTEX_POINT('',#56891);
#12490=VERTEX_POINT('',#56896);
#12491=VERTEX_POINT('',#56901);
#12492=VERTEX_POINT('',#56902);
#12493=VERTEX_POINT('',#56904);
#12494=VERTEX_POINT('',#56906);
#12495=VERTEX_POINT('',#56908);
#12496=VERTEX_POINT('',#56910);
#12497=VERTEX_POINT('',#56915);
#12498=VERTEX_POINT('',#56917);
#12499=VERTEX_POINT('',#56921);
#12500=VERTEX_POINT('',#56925);
#12501=VERTEX_POINT('',#56929);
#12502=VERTEX_POINT('',#56933);
#15887=EDGE_CURVE('',#12484,#12484,#10272,.T.);
#15888=EDGE_CURVE('',#12484,#12485,#7196,.T.);
#15889=EDGE_CURVE('',#12485,#12485,#10273,.T.);
#15890=EDGE_CURVE('',#12485,#12486,#7197,.T.);
#15891=EDGE_CURVE('',#12486,#12486,#10274,.T.);
#15892=EDGE_CURVE('',#12487,#12488,#10275,.T.);
#15893=EDGE_CURVE('',#12488,#12489,#7198,.T.);
#15894=EDGE_CURVE('',#12489,#12489,#10276,.T.);
#15895=EDGE_CURVE('',#12488,#12487,#10277,.T.);
#15896=EDGE_CURVE('',#12487,#12490,#7199,.T.);
#15897=EDGE_CURVE('',#12490,#12490,#10278,.T.);
#15898=EDGE_CURVE('',#12491,#12492,#7200,.T.);
#15899=EDGE_CURVE('',#12493,#12491,#7201,.T.);
#15900=EDGE_CURVE('',#12494,#12493,#7202,.T.);
#15901=EDGE_CURVE('',#12495,#12494,#7203,.T.);
#15902=EDGE_CURVE('',#12496,#12495,#7204,.T.);
#15903=EDGE_CURVE('',#12492,#12496,#7205,.T.);
#15904=EDGE_CURVE('',#12497,#12492,#7206,.T.);
#15905=EDGE_CURVE('',#12498,#12497,#7207,.T.);
#15906=EDGE_CURVE('',#12498,#12491,#7208,.T.);
#15907=EDGE_CURVE('',#12499,#12498,#7209,.T.);
#15908=EDGE_CURVE('',#12499,#12493,#7210,.T.);
#15909=EDGE_CURVE('',#12500,#12499,#7211,.T.);
#15910=EDGE_CURVE('',#12500,#12494,#7212,.T.);
#15911=EDGE_CURVE('',#12501,#12500,#7213,.T.);
#15912=EDGE_CURVE('',#12501,#12495,#7214,.T.);
#15913=EDGE_CURVE('',#12502,#12501,#7215,.T.);
#15914=EDGE_CURVE('',#12502,#12496,#7216,.T.);
#15915=EDGE_CURVE('',#12497,#12502,#7217,.T.);
#22684=ORIENTED_EDGE('',*,*,#15887,.F.);
#22685=ORIENTED_EDGE('',*,*,#15888,.T.);
#22686=ORIENTED_EDGE('',*,*,#15889,.T.);
#22687=ORIENTED_EDGE('',*,*,#15888,.F.);
#22688=ORIENTED_EDGE('',*,*,#15889,.F.);
#22689=ORIENTED_EDGE('',*,*,#15890,.T.);
#22690=ORIENTED_EDGE('',*,*,#15891,.T.);
#22691=ORIENTED_EDGE('',*,*,#15890,.F.);
#22692=ORIENTED_EDGE('',*,*,#15892,.T.);
#22693=ORIENTED_EDGE('',*,*,#15893,.T.);
#22694=ORIENTED_EDGE('',*,*,#15894,.F.);
#22695=ORIENTED_EDGE('',*,*,#15893,.F.);
#22696=ORIENTED_EDGE('',*,*,#15895,.T.);
#22697=ORIENTED_EDGE('',*,*,#15892,.F.);
#22698=ORIENTED_EDGE('',*,*,#15896,.T.);
#22699=ORIENTED_EDGE('',*,*,#15897,.T.);
#22700=ORIENTED_EDGE('',*,*,#15896,.F.);
#22701=ORIENTED_EDGE('',*,*,#15895,.F.);
#22702=ORIENTED_EDGE('',*,*,#15894,.T.);
#22703=ORIENTED_EDGE('',*,*,#15891,.F.);
#22704=ORIENTED_EDGE('',*,*,#15898,.F.);
#22705=ORIENTED_EDGE('',*,*,#15899,.F.);
#22706=ORIENTED_EDGE('',*,*,#15900,.F.);
#22707=ORIENTED_EDGE('',*,*,#15901,.F.);
#22708=ORIENTED_EDGE('',*,*,#15902,.F.);
#22709=ORIENTED_EDGE('',*,*,#15903,.F.);
#22710=ORIENTED_EDGE('',*,*,#15887,.T.);
#22711=ORIENTED_EDGE('',*,*,#15897,.F.);
#22712=ORIENTED_EDGE('',*,*,#15898,.T.);
#22713=ORIENTED_EDGE('',*,*,#15904,.F.);
#22714=ORIENTED_EDGE('',*,*,#15905,.F.);
#22715=ORIENTED_EDGE('',*,*,#15906,.T.);
#22716=ORIENTED_EDGE('',*,*,#15899,.T.);
#22717=ORIENTED_EDGE('',*,*,#15906,.F.);
#22718=ORIENTED_EDGE('',*,*,#15907,.F.);
#22719=ORIENTED_EDGE('',*,*,#15908,.T.);
#22720=ORIENTED_EDGE('',*,*,#15900,.T.);
#22721=ORIENTED_EDGE('',*,*,#15908,.F.);
#22722=ORIENTED_EDGE('',*,*,#15909,.F.);
#22723=ORIENTED_EDGE('',*,*,#15910,.T.);
#22724=ORIENTED_EDGE('',*,*,#15901,.T.);
#22725=ORIENTED_EDGE('',*,*,#15910,.F.);
#22726=ORIENTED_EDGE('',*,*,#15911,.F.);
#22727=ORIENTED_EDGE('',*,*,#15912,.T.);
#22728=ORIENTED_EDGE('',*,*,#15902,.T.);
#22729=ORIENTED_EDGE('',*,*,#15912,.F.);
#22730=ORIENTED_EDGE('',*,*,#15913,.F.);
#22731=ORIENTED_EDGE('',*,*,#15914,.T.);
#22732=ORIENTED_EDGE('',*,*,#15903,.T.);
#22733=ORIENTED_EDGE('',*,*,#15914,.F.);
#22734=ORIENTED_EDGE('',*,*,#15915,.F.);
#22735=ORIENTED_EDGE('',*,*,#15904,.T.);
#22736=ORIENTED_EDGE('',*,*,#15905,.T.);
#22737=ORIENTED_EDGE('',*,*,#15915,.T.);
#22738=ORIENTED_EDGE('',*,*,#15913,.T.);
#22739=ORIENTED_EDGE('',*,*,#15911,.T.);
#22740=ORIENTED_EDGE('',*,*,#15909,.T.);
#22741=ORIENTED_EDGE('',*,*,#15907,.T.);
#23149=CYLINDRICAL_SURFACE('',#27393,3.5);
#23150=CYLINDRICAL_SURFACE('',#27402,2.);
#24512=ADVANCED_FACE('',(#3520),#23149,.T.);
#24513=ADVANCED_FACE('',(#3521),#2157,.T.);
#24514=ADVANCED_FACE('',(#3522),#2158,.T.);
#24515=ADVANCED_FACE('',(#3523),#23150,.T.);
#24516=ADVANCED_FACE('',(#3524),#2095,.T.);
#24517=ADVANCED_FACE('',(#3525,#1340),#2096,.T.);
#24518=ADVANCED_FACE('',(#3526,#1341),#2097,.T.);
#24519=ADVANCED_FACE('',(#3527),#2098,.F.);
#24520=ADVANCED_FACE('',(#3528),#2099,.F.);
#24521=ADVANCED_FACE('',(#3529),#2100,.F.);
#24522=ADVANCED_FACE('',(#3530),#2101,.F.);
#24523=ADVANCED_FACE('',(#3531),#2102,.F.);
#24524=ADVANCED_FACE('',(#3532),#2103,.F.);
#24525=ADVANCED_FACE('',(#3533),#2104,.T.);
#24562=CLOSED_SHELL('',(#24512,#24513,#24514,#24515,#24516,#24517,#24518,
#24519,#24520,#24521,#24522,#24523,#24524,#24525));
#27392=AXIS2_PLACEMENT_3D('',#56876,#34440,#34441);
#27393=AXIS2_PLACEMENT_3D('',#56877,#34442,#34443);
#27394=AXIS2_PLACEMENT_3D('',#56879,#34444,#34445);
#27395=AXIS2_PLACEMENT_3D('',#56882,#34447,#34448);
#27396=AXIS2_PLACEMENT_3D('',#56883,#34449,#34450);
#27397=AXIS2_PLACEMENT_3D('',#56886,#34452,#34453);
#27398=AXIS2_PLACEMENT_3D('',#56887,#34454,#34455);
#27399=AXIS2_PLACEMENT_3D('',#56890,#34456,#34457);
#27400=AXIS2_PLACEMENT_3D('',#56893,#34459,#34460);
#27401=AXIS2_PLACEMENT_3D('',#56894,#34461,#34462);
#27402=AXIS2_PLACEMENT_3D('',#56895,#34463,#34464);
#27403=AXIS2_PLACEMENT_3D('',#56898,#34466,#34467);
#27404=AXIS2_PLACEMENT_3D('',#56899,#34468,#34469);
#27405=AXIS2_PLACEMENT_3D('',#56900,#34470,#34471);
#27406=AXIS2_PLACEMENT_3D('',#56913,#34478,#34479);
#27407=AXIS2_PLACEMENT_3D('',#56914,#34480,#34481);
#27408=AXIS2_PLACEMENT_3D('',#56920,#34485,#34486);
#27409=AXIS2_PLACEMENT_3D('',#56924,#34489,#34490);
#27410=AXIS2_PLACEMENT_3D('',#56928,#34493,#34494);
#27411=AXIS2_PLACEMENT_3D('',#56932,#34497,#34498);
#27412=AXIS2_PLACEMENT_3D('',#56936,#34501,#34502);
#27413=AXIS2_PLACEMENT_3D('',#56938,#34504,#34505);
#34440=DIRECTION('axis',(0.,0.,1.));
#34441=DIRECTION('refdir',(1.,0.,0.));
#34442=DIRECTION('center_axis',(1.,1.22464679914735E-16,0.));
#34443=DIRECTION('ref_axis',(-1.22464679914735E-16,1.,0.));
#34444=DIRECTION('center_axis',(1.,1.22464679914735E-16,0.));
#34445=DIRECTION('ref_axis',(-1.22464679914735E-16,1.,0.));
#34446=DIRECTION('',(-1.,-1.22464679914735E-16,0.));
#34447=DIRECTION('center_axis',(1.,1.22464679914735E-16,0.));
#34448=DIRECTION('ref_axis',(-1.22464679914735E-16,1.,0.));
#34449=DIRECTION('center_axis',(1.,1.22464679914735E-16,0.));
#34450=DIRECTION('ref_axis',(-1.22464679914735E-16,1.,0.));
#34451=DIRECTION('',(-0.707106781186548,0.707106781186547,8.65956056235492E-17));
#34452=DIRECTION('center_axis',(1.,1.22464679914735E-16,0.));
#34453=DIRECTION('ref_axis',(-1.22464679914735E-16,1.,0.));
#34454=DIRECTION('center_axis',(-1.,-1.22464679914735E-16,0.));
#34455=DIRECTION('ref_axis',(1.22464679914735E-16,-1.,0.));
#34456=DIRECTION('center_axis',(1.,1.22464679914735E-16,0.));
#34457=DIRECTION('ref_axis',(-1.22464679914735E-16,1.,0.));
#34458=DIRECTION('',(0.707106781186552,-0.707106781186543,8.65956056235488E-17));
#34459=DIRECTION('center_axis',(1.,1.22464679914735E-16,0.));
#34460=DIRECTION('ref_axis',(-1.22464679914735E-16,1.,0.));
#34461=DIRECTION('center_axis',(1.,1.22464679914735E-16,0.));
#34462=DIRECTION('ref_axis',(-1.22464679914735E-16,1.,0.));
#34463=DIRECTION('center_axis',(1.,1.22464679914735E-16,0.));
#34464=DIRECTION('ref_axis',(-1.22464679914735E-16,1.,0.));
#34465=DIRECTION('',(-1.,-1.22464679914735E-16,0.));
#34466=DIRECTION('center_axis',(1.,1.22464679914735E-16,0.));
#34467=DIRECTION('ref_axis',(-1.22464679914735E-16,1.,0.));
#34468=DIRECTION('center_axis',(1.,1.22464679914735E-16,0.));
#34469=DIRECTION('ref_axis',(-1.22464679914735E-16,1.,0.));
#34470=DIRECTION('center_axis',(-1.,-1.22464679914735E-16,0.));
#34471=DIRECTION('ref_axis',(1.22464679914735E-16,-1.,0.));
#34472=DIRECTION('',(0.,0.5,-0.866025403784439));
#34473=DIRECTION('',(0.,1.,2.50385766456193E-16));
#34474=DIRECTION('',(0.,0.5,0.866025403784439));
#34475=DIRECTION('',(0.,-0.5,0.866025403784438));
#34476=DIRECTION('',(0.,-1.,0.));
#34477=DIRECTION('',(0.,-0.5,-0.866025403784439));
#34478=DIRECTION('center_axis',(1.,1.22464679914735E-16,0.));
#34479=DIRECTION('ref_axis',(-1.22464679914735E-16,1.,0.));
#34480=DIRECTION('center_axis',(-1.06057523872491E-16,0.866025403784439,
0.5));
#34481=DIRECTION('ref_axis',(4.03425722881252E-33,-0.5,0.866025403784439));
#34482=DIRECTION('',(-1.,-1.22464679914735E-16,0.));
#34483=DIRECTION('',(0.,0.5,-0.866025403784439));
#34484=DIRECTION('',(-1.,-1.22464679914735E-16,0.));
#34485=DIRECTION('center_axis',(3.06634127442634E-32,-2.50385766456193E-16,
1.));
#34486=DIRECTION('ref_axis',(0.,-1.,-2.50385766456193E-16));
#34487=DIRECTION('',(0.,1.,2.50385766456193E-16));
#34488=DIRECTION('',(-1.,-1.22464679914735E-16,0.));
#34489=DIRECTION('center_axis',(1.06057523872491E-16,-0.866025403784439,
0.5));
#34490=DIRECTION('ref_axis',(-2.96989793219921E-33,-0.5,-0.866025403784439));
#34491=DIRECTION('',(0.,0.5,0.866025403784439));
#34492=DIRECTION('',(-1.,-1.22464679914735E-16,0.));
#34493=DIRECTION('center_axis',(1.06057523872491E-16,-0.866025403784439,
-0.5));
#34494=DIRECTION('ref_axis',(-4.03425722881252E-33,0.5,-0.866025403784439));
#34495=DIRECTION('',(0.,-0.5,0.866025403784438));
#34496=DIRECTION('',(-1.,-1.22464679914735E-16,0.));
#34497=DIRECTION('center_axis',(0.,0.,-1.));
#34498=DIRECTION('ref_axis',(-1.,0.,0.));
#34499=DIRECTION('',(0.,-1.,0.));
#34500=DIRECTION('',(-1.,-1.22464679914735E-16,0.));
#34501=DIRECTION('center_axis',(-1.06057523872491E-16,0.866025403784439,
-0.5));
#34502=DIRECTION('ref_axis',(4.03425722881253E-33,0.5,0.866025403784439));
#34503=DIRECTION('',(0.,-0.5,-0.866025403784439));
#34504=DIRECTION('center_axis',(-1.,0.,0.));
#34505=DIRECTION('ref_axis',(0.,0.,1.));
#56876=CARTESIAN_POINT('',(0.,0.,0.));
#56877=CARTESIAN_POINT('Origin',(20.,1.71450551880629E-15,0.));
#56878=CARTESIAN_POINT('',(0.,-3.5,-4.28626379701574E-16));
#56879=CARTESIAN_POINT('Origin',(0.,-7.34788079488412E-16,0.));
#56880=CARTESIAN_POINT('',(-3.6,-3.5,-4.28626379701574E-16));
#56881=CARTESIAN_POINT('',(20.,-3.5,-4.28626379701574E-16));
#56882=CARTESIAN_POINT('Origin',(-3.6,-1.17566092718146E-15,0.));
#56883=CARTESIAN_POINT('Origin',(-3.6,-1.17566092718146E-15,0.));
#56884=CARTESIAN_POINT('',(-4.,-3.1,-3.7964050773568E-16));
#56885=CARTESIAN_POINT('',(-3.6,-3.5,-4.28626379701574E-16));
#56886=CARTESIAN_POINT('Origin',(-4.,-1.22464679914735E-15,0.));
#56887=CARTESIAN_POINT('Origin',(20.,1.71450551880629E-15,0.));
#56888=CARTESIAN_POINT('',(19.621,-2.,2.4492935982947E-16));
#56889=CARTESIAN_POINT('',(19.621,2.,-2.4492935982947E-16));
#56890=CARTESIAN_POINT('Origin',(19.621,1.66809140511861E-15,0.));
#56891=CARTESIAN_POINT('',(20.,1.621,-1.98515246141786E-16));
#56892=CARTESIAN_POINT('',(20.,1.621,-1.98515246141786E-16));
#56893=CARTESIAN_POINT('Origin',(20.,1.71450551880629E-15,0.));
#56894=CARTESIAN_POINT('Origin',(19.621,1.66809140511861E-15,0.));
#56895=CARTESIAN_POINT('Origin',(20.,1.71450551880629E-15,0.));
#56896=CARTESIAN_POINT('',(0.,-2.,-2.44929359829471E-16));
#56897=CARTESIAN_POINT('',(20.,-2.,-2.44929359829471E-16));
#56898=CARTESIAN_POINT('Origin',(0.,-7.34788079488412E-16,0.));
#56899=CARTESIAN_POINT('Origin',(20.,1.621,0.));
#56900=CARTESIAN_POINT('Origin',(-4.,-1.22464679914735E-15,0.));
#56901=CARTESIAN_POINT('',(-4.,0.866025403784438,1.5));
#56902=CARTESIAN_POINT('',(-4.,1.73205080756888,1.0842021724855E-16));
#56903=CARTESIAN_POINT('',(-4.,0.866025403784438,1.5));
#56904=CARTESIAN_POINT('',(-4.,-0.866025403784439,1.5));
#56905=CARTESIAN_POINT('',(-4.,-0.866025403784439,1.5));
#56906=CARTESIAN_POINT('',(-4.,-1.73205080756888,-5.3318781527803E-16));
#56907=CARTESIAN_POINT('',(-4.,-1.73205080756888,-5.3318781527803E-16));
#56908=CARTESIAN_POINT('',(-4.,-0.866025403784439,-1.5));
#56909=CARTESIAN_POINT('',(-4.,-0.866025403784439,-1.5));
#56910=CARTESIAN_POINT('',(-4.,0.866025403784438,-1.5));
#56911=CARTESIAN_POINT('',(-4.,0.866025403784438,-1.5));
#56912=CARTESIAN_POINT('',(-4.,1.73205080756888,1.43478627046003E-16));
#56913=CARTESIAN_POINT('Origin',(9.18485099360515E-17,2.,0.));
#56914=CARTESIAN_POINT('Origin',(-2.,0.866025403784439,1.5));
#56915=CARTESIAN_POINT('',(-2.,1.73205080756888,1.43478627046003E-16));
#56916=CARTESIAN_POINT('',(-2.,1.73205080756888,1.43478627046003E-16));
#56917=CARTESIAN_POINT('',(-2.,0.866025403784439,1.5));
#56918=CARTESIAN_POINT('',(-2.,0.866025403784439,1.5));
#56919=CARTESIAN_POINT('',(-2.,0.866025403784439,1.5));
#56920=CARTESIAN_POINT('Origin',(-2.,-0.866025403784439,1.5));
#56921=CARTESIAN_POINT('',(-2.,-0.866025403784439,1.5));
#56922=CARTESIAN_POINT('',(-2.,-0.866025403784439,1.5));
#56923=CARTESIAN_POINT('',(-2.,-0.866025403784439,1.5));
#56924=CARTESIAN_POINT('Origin',(-2.,-1.73205080756888,-5.3318781527803E-16));
#56925=CARTESIAN_POINT('',(-2.,-1.73205080756888,-5.3318781527803E-16));
#56926=CARTESIAN_POINT('',(-2.,-1.73205080756888,-5.3318781527803E-16));
#56927=CARTESIAN_POINT('',(-2.,-1.73205080756888,-5.3318781527803E-16));
#56928=CARTESIAN_POINT('Origin',(-2.,-0.866025403784439,-1.5));
#56929=CARTESIAN_POINT('',(-2.,-0.866025403784439,-1.5));
#56930=CARTESIAN_POINT('',(-2.,-0.866025403784439,-1.5));
#56931=CARTESIAN_POINT('',(-2.,-0.866025403784439,-1.5));
#56932=CARTESIAN_POINT('Origin',(-2.,0.866025403784439,-1.5));
#56933=CARTESIAN_POINT('',(-2.,0.866025403784439,-1.5));
#56934=CARTESIAN_POINT('',(-2.,0.866025403784439,-1.5));
#56935=CARTESIAN_POINT('',(-2.,0.866025403784439,-1.5));
#56936=CARTESIAN_POINT('Origin',(-2.,1.73205080756888,1.43478627046003E-16));
#56937=CARTESIAN_POINT('',(-2.,1.73205080756888,1.43478627046003E-16));
#56938=CARTESIAN_POINT('Origin',(-2.,2.44929359829471E-16,0.));
#57039=UNCERTAINTY_MEASURE_WITH_UNIT(LENGTH_MEASURE(0.01),#57080,
'DISTANCE_ACCURACY_VALUE',
'Maximum model space distance between geometric entities at asserted c
onnectivities');
#57040=UNCERTAINTY_MEASURE_WITH_UNIT(LENGTH_MEASURE(0.01),#57080,
'DISTANCE_ACCURACY_VALUE',
'Maximum model space distance between geometric entities at asserted c
onnectivities');
#57078=(
GEOMETRIC_REPRESENTATION_CONTEXT(3)
GLOBAL_UNCERTAINTY_ASSIGNED_CONTEXT((#57039))
GLOBAL_UNIT_ASSIGNED_CONTEXT((#57080,#57082,#57083))
REPRESENTATION_CONTEXT('','3D')
);
#57079=(
GEOMETRIC_REPRESENTATION_CONTEXT(3)
GLOBAL_UNCERTAINTY_ASSIGNED_CONTEXT((#57040))
GLOBAL_UNIT_ASSIGNED_CONTEXT((#57080,#57082,#57083))
REPRESENTATION_CONTEXT('','3D')
);
#57080=(
LENGTH_UNIT()
NAMED_UNIT(*)
SI_UNIT(.MILLI.,.METRE.)
);
#57082=(
NAMED_UNIT(*)
PLANE_ANGLE_UNIT()
SI_UNIT($,.RADIAN.)
);
#57083=(
NAMED_UNIT(*)
SI_UNIT($,.STERADIAN.)
SOLID_ANGLE_UNIT()
);
#57121=SHAPE_DEFINITION_REPRESENTATION(#57185,#57286);
#57185=PRODUCT_DEFINITION_SHAPE('',$,#57325);
#57286=SHAPE_REPRESENTATION('',(#27392),#57078);
#57287=PRODUCT_DEFINITION_CONTEXT('part definition',#57403,'design');
#57325=PRODUCT_DEFINITION('Socket head cap screw M4x20',
'Socket Head Cap Screw M4x20',#57363,#57287);
#57363=PRODUCT_DEFINITION_FORMATION('',$,#57442);
#57403=APPLICATION_CONTEXT(
'Core Data for Automotive Mechanical Design Process');
#57404=PRODUCT_CONTEXT('part definition',#57403,'mechanical');
#57442=PRODUCT('Socket head cap screw M4x20',
'Socket Head Cap Screw M4x20',$,(#57404));
#57444=PRESENTATION_STYLE_ASSIGNMENT((#57446));
#57446=SURFACE_STYLE_USAGE(.BOTH.,#57448);
#57448=SURFACE_SIDE_STYLE('',(#57450));
#57450=SURFACE_STYLE_FILL_AREA(#57452);
#57452=FILL_AREA_STYLE('Opaque(202,209,238)',(#57454));
#57454=FILL_AREA_STYLE_COLOUR('Opaque(202,209,238)',#57456);
#57456=COLOUR_RGB('Opaque(202,209,238)',0.792156862745098,0.819607843137255,
0.933333333333333);
ENDSEC;
END-ISO-10303-21;
